ISO-10303-21;
HEADER;
/* Generated by software containing ST-Developer
 * from STEP Tools, Inc. (www.steptools.com) 
 */

FILE_DESCRIPTION(
/* description */ ('Cylinder foot and clevis mount kit'),
/* implementation_level */ '2;1');

FILE_NAME(
/* name */ 'Cap Screw - M4x16.step',
/* time_stamp */ '2026-10-27T20:10:43-07:00',
/* author */ (''),
/* organization */ (''),
/* preprocessor_version */ 'ST-DEVELOPER v20.2',
/* originating_system */ 'Autodesk Translation Framework v15.17.0.0',
/* authorisation */ '');

FILE_SCHEMA (('AUTOMOTIVE_DESIGN { 1 0 10303 214 3 1 1 }'));
ENDSEC;

DATA;
#10=MECHANICAL_DESIGN_GEOMETRIC_PRESENTATION_REPRESENTATION('',(#360),#9102);
#260=ORIENTED_CLOSED_SHELL('',*,#4948,.F.);
#262=BREP_WITH_VOIDS('Body1',#4947,(#260));
#274=CONICAL_SURFACE('',#5776,0.325,0.785398163397448);
#275=CONICAL_SURFACE('',#5780,0.335,0.785398163397448);
#276=CONICAL_SURFACE('',#5784,0.21,0.463647609000806);
#277=CONICAL_SURFACE('',#5788,0.18,0.785398163397448);
#304=SHAPE_REPRESENTATION_RELATIONSHIP('SRR','None',#9253,#332);
#332=ADVANCED_BREP_SHAPE_REPRESENTATION('',(#262),#9096);
#360=STYLED_ITEM('',(#9467),#262);
#480=FACE_BOUND('',#1338,.T.);
#655=PLANE('',#5774);
#656=PLANE('',#5782);
#657=PLANE('',#5790);
#658=PLANE('',#5791);
#659=PLANE('',#5792);
#660=PLANE('',#5793);
#661=PLANE('',#5794);
#662=PLANE('',#5795);
#663=PLANE('',#5796);
#664=PLANE('',#5797);
#665=PLANE('',#5798);
#939=FACE_OUTER_BOUND('',#1333,.T.);
#940=FACE_OUTER_BOUND('',#1334,.T.);
#941=FACE_OUTER_BOUND('',#1335,.T.);
#942=FACE_OUTER_BOUND('',#1336,.T.);
#943=FACE_OUTER_BOUND('',#1337,.T.);
#944=FACE_OUTER_BOUND('',#1339,.T.);
#945=FACE_OUTER_BOUND('',#1340,.T.);
#946=FACE_OUTER_BOUND('',#1341,.T.);
#947=FACE_OUTER_BOUND('',#1342,.T.);
#948=FACE_OUTER_BOUND('',#1343,.T.);
#949=FACE_OUTER_BOUND('',#1344,.T.);
#950=FACE_OUTER_BOUND('',#1345,.T.);
#951=FACE_OUTER_BOUND('',#1346,.T.);
#952=FACE_OUTER_BOUND('',#1347,.T.);
#953=FACE_OUTER_BOUND('',#1348,.T.);
#954=FACE_OUTER_BOUND('',#1349,.T.);
#955=FACE_OUTER_BOUND('',#1350,.T.);
#1333=EDGE_LOOP('',(#4255));
#1334=EDGE_LOOP('',(#4256,#4257,#4258,#4259));
#1335=EDGE_LOOP('',(#4260,#4261,#4262,#4263));
#1336=EDGE_LOOP('',(#4264,#4265,#4266,#4267));
#1337=EDGE_LOOP('',(#4268));
#1338=EDGE_LOOP('',(#4269));
#1339=EDGE_LOOP('',(#4270,#4271,#4272,#4273));
#1340=EDGE_LOOP('',(#4274,#4275,#4276,#4277));
#1341=EDGE_LOOP('',(#4278,#4279,#4280,#4281));
#1342=EDGE_LOOP('',(#4282));
#1343=EDGE_LOOP('',(#4283,#4284,#4285,#4286));
#1344=EDGE_LOOP('',(#4287,#4288,#4289,#4290));
#1345=EDGE_LOOP('',(#4291,#4292,#4293,#4294));
#1346=EDGE_LOOP('',(#4295,#4296,#4297,#4298));
#1347=EDGE_LOOP('',(#4299,#4300,#4301,#4302));
#1348=EDGE_LOOP('',(#4303,#4304,#4305,#4306));
#1349=EDGE_LOOP('',(#4307,#4308,#4309,#4310,#4311,#4312));
#1350=EDGE_LOOP('',(#4313,#4314,#4315,#4316,#4317,#4318));
#1671=LINE('',#8608,#2020);
#1672=LINE('',#8612,#2021);
#1673=LINE('',#8616,#2022);
#1674=LINE('',#8623,#2023);
#1675=LINE('',#8627,#2024);
#1676=LINE('',#8631,#2025);
#1677=LINE('',#8636,#2026);
#1678=LINE('',#8638,#2027);
#1679=LINE('',#8640,#2028);
#1680=LINE('',#8641,#2029);
#1681=LINE('',#8644,#2030);
#1682=LINE('',#8646,#2031);
#1683=LINE('',#8647,#2032);
#1684=LINE('',#8650,#2033);
#1685=LINE('',#8652,#2034);
#1686=LINE('',#8653,#2035);
#1687=LINE('',#8656,#2036);
#1688=LINE('',#8658,#2037);
#1689=LINE('',#8659,#2038);
#1690=LINE('',#8662,#2039);
#1691=LINE('',#8664,#2040);
#1692=LINE('',#8665,#2041);
#1693=LINE('',#8667,#2042);
#1694=LINE('',#8668,#2043);
#2020=VECTOR('',#7182,0.325);
#2021=VECTOR('',#7187,0.35);
#2022=VECTOR('',#7192,0.335);
#2023=VECTOR('',#7201,0.21);
#2024=VECTOR('',#7206,0.2);
#2025=VECTOR('',#7211,0.18);
#2026=VECTOR('',#7216,1.);
#2027=VECTOR('',#7217,1.);
#2028=VECTOR('',#7218,1.);
#2029=VECTOR('',#7219,1.);
#2030=VECTOR('',#7222,1.);
#2031=VECTOR('',#7223,1.);
#2032=VECTOR('',#7224,1.);
#2033=VECTOR('',#7227,1.);
#2034=VECTOR('',#7228,1.);
#2035=VECTOR('',#7229,1.);
#2036=VECTOR('',#7232,1.);
#2037=VECTOR('',#7233,1.);
#2038=VECTOR('',#7234,1.);
#2039=VECTOR('',#7237,1.);
#2040=VECTOR('',#7238,1.);
#2041=VECTOR('',#7239,1.);
#2042=VECTOR('',#7242,1.);
#2043=VECTOR('',#7243,1.);
#2291=CIRCLE('',#5775,0.3);
#2292=CIRCLE('',#5777,0.35);
#2293=CIRCLE('',#5779,0.35);
#2294=CIRCLE('',#5781,0.32);
#2295=CIRCLE('',#5783,0.22);
#2296=CIRCLE('',#5785,0.1954);
#2297=CIRCLE('',#5787,0.1954);
#2298=CIRCLE('',#5789,0.16);
#2626=VERTEX_POINT('',#8603);
#2627=VERTEX_POINT('',#8606);
#2628=VERTEX_POINT('',#8610);
#2629=VERTEX_POINT('',#8614);
#2630=VERTEX_POINT('',#8618);
#2631=VERTEX_POINT('',#8621);
#2632=VERTEX_POINT('',#8625);
#2633=VERTEX_POINT('',#8629);
#2634=VERTEX_POINT('',#8634);
#2635=VERTEX_POINT('',#8635);
#2636=VERTEX_POINT('',#8637);
#2637=VERTEX_POINT('',#8639);
#2638=VERTEX_POINT('',#8643);
#2639=VERTEX_POINT('',#8645);
#2640=VERTEX_POINT('',#8649);
#2641=VERTEX_POINT('',#8651);
#2642=VERTEX_POINT('',#8655);
#2643=VERTEX_POINT('',#8657);
#2644=VERTEX_POINT('',#8661);
#2645=VERTEX_POINT('',#8663);
#3182=EDGE_CURVE('',#2626,#2626,#2291,.T.);
#3183=EDGE_CURVE('',#2627,#2627,#2292,.T.);
#3184=EDGE_CURVE('',#2627,#2626,#1671,.T.);
#3185=EDGE_CURVE('',#2628,#2628,#2293,.T.);
#3186=EDGE_CURVE('',#2628,#2627,#1672,.T.);
#3187=EDGE_CURVE('',#2629,#2629,#2294,.T.);
#3188=EDGE_CURVE('',#2629,#2628,#1673,.T.);
#3189=EDGE_CURVE('',#2630,#2630,#2295,.T.);
#3190=EDGE_CURVE('',#2631,#2631,#2296,.F.);
#3191=EDGE_CURVE('',#2631,#2630,#1674,.T.);
#3192=EDGE_CURVE('',#2632,#2632,#2297,.F.);
#3193=EDGE_CURVE('',#2632,#2631,#1675,.T.);
#3194=EDGE_CURVE('',#2633,#2633,#2298,.T.);
#3195=EDGE_CURVE('',#2633,#2632,#1676,.T.);
#3196=EDGE_CURVE('',#2634,#2635,#1677,.T.);
#3197=EDGE_CURVE('',#2635,#2636,#1678,.T.);
#3198=EDGE_CURVE('',#2636,#2637,#1679,.T.);
#3199=EDGE_CURVE('',#2634,#2637,#1680,.T.);
#3200=EDGE_CURVE('',#2635,#2638,#1681,.T.);
#3201=EDGE_CURVE('',#2638,#2639,#1682,.T.);
#3202=EDGE_CURVE('',#2639,#2636,#1683,.T.);
#3203=EDGE_CURVE('',#2638,#2640,#1684,.T.);
#3204=EDGE_CURVE('',#2640,#2641,#1685,.T.);
#3205=EDGE_CURVE('',#2641,#2639,#1686,.T.);
#3206=EDGE_CURVE('',#2640,#2642,#1687,.T.);
#3207=EDGE_CURVE('',#2642,#2643,#1688,.T.);
#3208=EDGE_CURVE('',#2643,#2641,#1689,.T.);
#3209=EDGE_CURVE('',#2642,#2644,#1690,.T.);
#3210=EDGE_CURVE('',#2644,#2645,#1691,.T.);
#3211=EDGE_CURVE('',#2645,#2643,#1692,.T.);
#3212=EDGE_CURVE('',#2644,#2634,#1693,.T.);
#3213=EDGE_CURVE('',#2637,#2645,#1694,.T.);
#4255=ORIENTED_EDGE('',*,*,#3182,.F.);
#4256=ORIENTED_EDGE('',*,*,#3183,.F.);
#4257=ORIENTED_EDGE('',*,*,#3184,.T.);
#4258=ORIENTED_EDGE('',*,*,#3182,.T.);
#4259=ORIENTED_EDGE('',*,*,#3184,.F.);
#4260=ORIENTED_EDGE('',*,*,#3185,.F.);
#4261=ORIENTED_EDGE('',*,*,#3186,.T.);
#4262=ORIENTED_EDGE('',*,*,#3183,.T.);
#4263=ORIENTED_EDGE('',*,*,#3186,.F.);
#4264=ORIENTED_EDGE('',*,*,#3187,.F.);
#4265=ORIENTED_EDGE('',*,*,#3188,.T.);
#4266=ORIENTED_EDGE('',*,*,#3185,.T.);
#4267=ORIENTED_EDGE('',*,*,#3188,.F.);
#4268=ORIENTED_EDGE('',*,*,#3187,.T.);
#4269=ORIENTED_EDGE('',*,*,#3189,.F.);
#4270=ORIENTED_EDGE('',*,*,#3190,.F.);
#4271=ORIENTED_EDGE('',*,*,#3191,.T.);
#4272=ORIENTED_EDGE('',*,*,#3189,.T.);
#4273=ORIENTED_EDGE('',*,*,#3191,.F.);
#4274=ORIENTED_EDGE('',*,*,#3192,.F.);
#4275=ORIENTED_EDGE('',*,*,#3193,.T.);
#4276=ORIENTED_EDGE('',*,*,#3190,.T.);
#4277=ORIENTED_EDGE('',*,*,#3193,.F.);
#4278=ORIENTED_EDGE('',*,*,#3194,.F.);
#4279=ORIENTED_EDGE('',*,*,#3195,.T.);
#4280=ORIENTED_EDGE('',*,*,#3192,.T.);
#4281=ORIENTED_EDGE('',*,*,#3195,.F.);
#4282=ORIENTED_EDGE('',*,*,#3194,.T.);
#4283=ORIENTED_EDGE('',*,*,#3196,.T.);
#4284=ORIENTED_EDGE('',*,*,#3197,.T.);
#4285=ORIENTED_EDGE('',*,*,#3198,.T.);
#4286=ORIENTED_EDGE('',*,*,#3199,.F.);
#4287=ORIENTED_EDGE('',*,*,#3200,.T.);
#4288=ORIENTED_EDGE('',*,*,#3201,.T.);
#4289=ORIENTED_EDGE('',*,*,#3202,.T.);
#4290=ORIENTED_EDGE('',*,*,#3197,.F.);
#4291=ORIENTED_EDGE('',*,*,#3203,.T.);
#4292=ORIENTED_EDGE('',*,*,#3204,.T.);
#4293=ORIENTED_EDGE('',*,*,#3205,.T.);
#4294=ORIENTED_EDGE('',*,*,#3201,.F.);
#4295=ORIENTED_EDGE('',*,*,#3206,.T.);
#4296=ORIENTED_EDGE('',*,*,#3207,.T.);
#4297=ORIENTED_EDGE('',*,*,#3208,.T.);
#4298=ORIENTED_EDGE('',*,*,#3204,.F.);
#4299=ORIENTED_EDGE('',*,*,#3209,.T.);
#4300=ORIENTED_EDGE('',*,*,#3210,.T.);
#4301=ORIENTED_EDGE('',*,*,#3211,.T.);
#4302=ORIENTED_EDGE('',*,*,#3207,.F.);
#4303=ORIENTED_EDGE('',*,*,#3212,.T.);
#4304=ORIENTED_EDGE('',*,*,#3199,.T.);
#4305=ORIENTED_EDGE('',*,*,#3213,.T.);
#4306=ORIENTED_EDGE('',*,*,#3210,.F.);
#4307=ORIENTED_EDGE('',*,*,#3212,.F.);
#4308=ORIENTED_EDGE('',*,*,#3209,.F.);
#4309=ORIENTED_EDGE('',*,*,#3206,.F.);
#4310=ORIENTED_EDGE('',*,*,#3203,.F.);
#4311=ORIENTED_EDGE('',*,*,#3200,.F.);
#4312=ORIENTED_EDGE('',*,*,#3196,.F.);
#4313=ORIENTED_EDGE('',*,*,#3213,.F.);
#4314=ORIENTED_EDGE('',*,*,#3198,.F.);
#4315=ORIENTED_EDGE('',*,*,#3202,.F.);
#4316=ORIENTED_EDGE('',*,*,#3205,.F.);
#4317=ORIENTED_EDGE('',*,*,#3208,.F.);
#4318=ORIENTED_EDGE('',*,*,#3211,.F.);
#4605=CYLINDRICAL_SURFACE('',#5778,0.35);
#4606=CYLINDRICAL_SURFACE('',#5786,0.1954);
#4862=ADVANCED_FACE('',(#939),#655,.T.);
#4863=ADVANCED_FACE('',(#940),#274,.T.);
#4864=ADVANCED_FACE('',(#941),#4605,.T.);
#4865=ADVANCED_FACE('',(#942),#275,.T.);
#4866=ADVANCED_FACE('',(#943,#480),#656,.T.);
#4867=ADVANCED_FACE('',(#944),#276,.T.);
#4868=ADVANCED_FACE('',(#945),#4606,.T.);
#4869=ADVANCED_FACE('',(#946),#277,.T.);
#4870=ADVANCED_FACE('',(#947),#657,.T.);
#4871=ADVANCED_FACE('',(#948),#658,.F.);
#4872=ADVANCED_FACE('',(#949),#659,.F.);
#4873=ADVANCED_FACE('',(#950),#660,.F.);
#4874=ADVANCED_FACE('',(#951),#661,.F.);
#4875=ADVANCED_FACE('',(#952),#662,.F.);
#4876=ADVANCED_FACE('',(#953),#663,.F.);
#4877=ADVANCED_FACE('',(#954),#664,.F.);
#4878=ADVANCED_FACE('',(#955),#665,.F.);
#4947=CLOSED_SHELL('',(#4862,#4863,#4864,#4865,#4866,#4867,#4868,#4869,
#4870));
#4948=CLOSED_SHELL('',(#4871,#4872,#4873,#4874,#4875,#4876,#4877,#4878));
#5773=AXIS2_PLACEMENT_3D('',#8601,#7172,#7173);
#5774=AXIS2_PLACEMENT_3D('',#8602,#7174,#7175);
#5775=AXIS2_PLACEMENT_3D('',#8604,#7176,#7177);
#5776=AXIS2_PLACEMENT_3D('',#8605,#7178,#7179);
#5777=AXIS2_PLACEMENT_3D('',#8607,#7180,#7181);
#5778=AXIS2_PLACEMENT_3D('',#8609,#7183,#7184);
#5779=AXIS2_PLACEMENT_3D('',#8611,#7185,#7186);
#5780=AXIS2_PLACEMENT_3D('',#8613,#7188,#7189);
#5781=AXIS2_PLACEMENT_3D('',#8615,#7190,#7191);
#5782=AXIS2_PLACEMENT_3D('',#8617,#7193,#7194);
#5783=AXIS2_PLACEMENT_3D('',#8619,#7195,#7196);
#5784=AXIS2_PLACEMENT_3D('',#8620,#7197,#7198);
#5785=AXIS2_PLACEMENT_3D('',#8622,#7199,#7200);
#5786=AXIS2_PLACEMENT_3D('',#8624,#7202,#7203);
#5787=AXIS2_PLACEMENT_3D('',#8626,#7204,#7205);
#5788=AXIS2_PLACEMENT_3D('',#8628,#7207,#7208);
#5789=AXIS2_PLACEMENT_3D('',#8630,#7209,#7210);
#5790=AXIS2_PLACEMENT_3D('',#8632,#7212,#7213);
#5791=AXIS2_PLACEMENT_3D('',#8633,#7214,#7215);
#5792=AXIS2_PLACEMENT_3D('',#8642,#7220,#7221);
#5793=AXIS2_PLACEMENT_3D('',#8648,#7225,#7226);
#5794=AXIS2_PLACEMENT_3D('',#8654,#7230,#7231);
#5795=AXIS2_PLACEMENT_3D('',#8660,#7235,#7236);
#5796=AXIS2_PLACEMENT_3D('',#8666,#7240,#7241);
#5797=AXIS2_PLACEMENT_3D('',#8669,#7244,#7245);
#5798=AXIS2_PLACEMENT_3D('',#8670,#7246,#7247);
#7172=DIRECTION('axis',(0.,0.,1.));
#7173=DIRECTION('refdir',(1.,0.,0.));
#7174=DIRECTION('center_axis',(0.,1.,0.));
#7175=DIRECTION('ref_axis',(0.,0.,1.));
#7176=DIRECTION('center_axis',(0.,-1.,0.));
#7177=DIRECTION('ref_axis',(1.,0.,0.));
#7178=DIRECTION('center_axis',(0.,-1.,0.));
#7179=DIRECTION('ref_axis',(1.,0.,0.));
#7180=DIRECTION('center_axis',(0.,-1.,0.));
#7181=DIRECTION('ref_axis',(1.,0.,0.));
#7182=DIRECTION('',(0.707106781186547,0.707106781186548,8.65956056235493E-17));
#7183=DIRECTION('center_axis',(0.,-1.,0.));
#7184=DIRECTION('ref_axis',(1.,0.,0.));
#7185=DIRECTION('center_axis',(0.,-1.,0.));
#7186=DIRECTION('ref_axis',(1.,0.,0.));
#7187=DIRECTION('',(0.,1.,0.));
#7188=DIRECTION('center_axis',(0.,1.,0.));
#7189=DIRECTION('ref_axis',(1.,0.,0.));
#7190=DIRECTION('center_axis',(0.,-1.,0.));
#7191=DIRECTION('ref_axis',(1.,0.,0.));
#7192=DIRECTION('',(-0.707106781186547,0.707106781186548,-8.65956056235493E-17));
#7193=DIRECTION('center_axis',(0.,-1.,0.));
#7194=DIRECTION('ref_axis',(0.,0.,-1.));
#7195=DIRECTION('center_axis',(0.,-1.,0.));
#7196=DIRECTION('ref_axis',(1.,0.,0.));
#7197=DIRECTION('center_axis',(0.,1.,0.));
#7198=DIRECTION('ref_axis',(1.,0.,0.));
#7199=DIRECTION('center_axis',(0.,1.,0.));
#7200=DIRECTION('ref_axis',(1.,0.,0.));
#7201=DIRECTION('',(-0.447213595499958,0.894427190999916,-5.47678698264203E-17));
#7202=DIRECTION('center_axis',(0.,-1.,0.));
#7203=DIRECTION('ref_axis',(1.,0.,0.));
#7204=DIRECTION('center_axis',(0.,1.,0.));
#7205=DIRECTION('ref_axis',(1.,0.,0.));
#7206=DIRECTION('',(0.,1.,0.));
#7207=DIRECTION('center_axis',(0.,1.,0.));
#7208=DIRECTION('ref_axis',(1.,0.,0.));
#7209=DIRECTION('center_axis',(0.,-1.,0.));
#7210=DIRECTION('ref_axis',(1.,0.,0.));
#7211=DIRECTION('',(-0.707106781186547,0.707106781186548,-8.65956056235493E-17));
#7212=DIRECTION('center_axis',(0.,-1.,0.));
#7213=DIRECTION('ref_axis',(0.,0.,-1.));
#7214=DIRECTION('center_axis',(0.866025403784439,0.,-0.5));
#7215=DIRECTION('ref_axis',(0.5,0.,0.866025403784439));
#7216=DIRECTION('',(-0.5,0.,-0.866025403784439));
#7217=DIRECTION('',(0.,-1.,0.));
#7218=DIRECTION('',(0.5,0.,0.866025403784439));
#7219=DIRECTION('',(0.,-1.,0.));
#7220=DIRECTION('center_axis',(1.60246890531964E-16,0.,-1.));
#7221=DIRECTION('ref_axis',(1.,0.,1.60246890531964E-16));
#7222=DIRECTION('',(-1.,0.,-1.60246890531964E-16));
#7223=DIRECTION('',(0.,-1.,0.));
#7224=DIRECTION('',(1.,0.,1.60246890531964E-16));
#7225=DIRECTION('center_axis',(-0.866025403784439,0.,-0.5));
#7226=DIRECTION('ref_axis',(0.5,0.,-0.866025403784439));
#7227=DIRECTION('',(-0.5,0.,0.866025403784439));
#7228=DIRECTION('',(0.,-1.,0.));
#7229=DIRECTION('',(0.5,0.,-0.866025403784439));
#7230=DIRECTION('center_axis',(-0.866025403784439,0.,0.5));
#7231=DIRECTION('ref_axis',(-0.5,0.,-0.866025403784439));
#7232=DIRECTION('',(0.5,0.,0.866025403784439));
#7233=DIRECTION('',(0.,-1.,0.));
#7234=DIRECTION('',(-0.5,0.,-0.866025403784439));
#7235=DIRECTION('center_axis',(-1.60246890531964E-16,0.,1.));
#7236=DIRECTION('ref_axis',(-1.,0.,-1.60246890531964E-16));
#7237=DIRECTION('',(1.,0.,1.60246890531964E-16));
#7238=DIRECTION('',(0.,-1.,0.));
#7239=DIRECTION('',(-1.,0.,-1.60246890531964E-16));
#7240=DIRECTION('center_axis',(0.866025403784439,0.,0.5));
#7241=DIRECTION('ref_axis',(-0.5,0.,0.866025403784439));
#7242=DIRECTION('',(0.5,0.,-0.866025403784439));
#7243=DIRECTION('',(-0.5,0.,0.866025403784439));
#7244=DIRECTION('center_axis',(0.,1.,0.));
#7245=DIRECTION('ref_axis',(1.,0.,0.));
#7246=DIRECTION('center_axis',(0.,-1.,0.));
#7247=DIRECTION('ref_axis',(0.,0.,-1.));
#8601=CARTESIAN_POINT('',(0.,0.,0.));
#8602=CARTESIAN_POINT('Origin',(0.3,0.4,0.));
#8603=CARTESIAN_POINT('',(-0.3,0.4,-3.67394039744206E-17));
#8604=CARTESIAN_POINT('Origin',(0.,0.4,0.));
#8605=CARTESIAN_POINT('Origin',(0.,0.375,0.));
#8606=CARTESIAN_POINT('',(-0.35,0.35,-4.28626379701573E-17));
#8607=CARTESIAN_POINT('Origin',(0.,0.35,0.));
#8608=CARTESIAN_POINT('',(-0.325,0.375,-3.9801020972289E-17));
#8609=CARTESIAN_POINT('Origin',(0.,0.19,0.));
#8610=CARTESIAN_POINT('',(-0.35,0.03,-4.28626379701574E-17));
#8611=CARTESIAN_POINT('Origin',(0.,0.03,0.));
#8612=CARTESIAN_POINT('',(-0.35,0.19,-4.28626379701574E-17));
#8613=CARTESIAN_POINT('Origin',(0.,0.0149999999999999,0.));
#8614=CARTESIAN_POINT('',(-0.32,-3.29597460435593E-17,-3.91886975727153E-17));
#8615=CARTESIAN_POINT('Origin',(0.,0.,0.));
#8616=CARTESIAN_POINT('',(-0.335,0.0149999999999999,-4.10256677714363E-17));
#8617=CARTESIAN_POINT('Origin',(0.22,0.,0.));
#8618=CARTESIAN_POINT('',(-0.22,-6.93889390390723E-18,-2.69422295812418E-17));
#8619=CARTESIAN_POINT('Origin',(0.,0.,0.));
#8620=CARTESIAN_POINT('Origin',(0.,-0.02,0.));
#8621=CARTESIAN_POINT('',(-0.1954,-0.0492,2.39295984553393E-17));
#8622=CARTESIAN_POINT('Origin',(0.,-0.0492,0.));
#8623=CARTESIAN_POINT('',(-0.21,-0.02,-2.57175827820944E-17));
#8624=CARTESIAN_POINT('Origin',(0.,-0.8,0.));
#8625=CARTESIAN_POINT('',(-0.1954,-1.5646,2.39295984553393E-17));
#8626=CARTESIAN_POINT('Origin',(0.,-1.5646,0.));
#8627=CARTESIAN_POINT('',(-0.1954,-0.8,-2.39295984553393E-17));
#8628=CARTESIAN_POINT('Origin',(0.,-1.58,0.));
#8629=CARTESIAN_POINT('',(-0.16,-1.6,-1.95943487863577E-17));
#8630=CARTESIAN_POINT('Origin',(0.,-1.6,0.));
#8631=CARTESIAN_POINT('',(-0.18,-1.58,-2.20436423846524E-17));
#8632=CARTESIAN_POINT('Origin',(0.,-1.6,0.));
#8633=CARTESIAN_POINT('Origin',(0.0866025403784439,-0.4,-0.15));
#8634=CARTESIAN_POINT('',(0.173205080756888,-0.4,0.));
#8635=CARTESIAN_POINT('',(0.0866025403784439,-0.4,-0.15));
#8636=CARTESIAN_POINT('',(0.173205080756888,-0.4,0.));
#8637=CARTESIAN_POINT('',(0.0866025403784439,-0.64,-0.15));
#8638=CARTESIAN_POINT('',(0.0866025403784439,-0.4,-0.15));
#8639=CARTESIAN_POINT('',(0.173205080756888,-0.64,0.));
#8640=CARTESIAN_POINT('',(0.173205080756888,-0.64,0.));
#8641=CARTESIAN_POINT('',(0.173205080756888,-0.4,0.));
#8642=CARTESIAN_POINT('Origin',(-0.0866025403784438,-0.4,-0.15));
#8643=CARTESIAN_POINT('',(-0.0866025403784438,-0.4,-0.15));
#8644=CARTESIAN_POINT('',(0.0866025403784439,-0.4,-0.15));
#8645=CARTESIAN_POINT('',(-0.0866025403784438,-0.64,-0.15));
#8646=CARTESIAN_POINT('',(-0.0866025403784438,-0.4,-0.15));
#8647=CARTESIAN_POINT('',(0.0866025403784439,-0.64,-0.15));
#8648=CARTESIAN_POINT('Origin',(-0.173205080756888,-0.4,-2.77555756156289E-17));
#8649=CARTESIAN_POINT('',(-0.173205080756888,-0.4,-2.12115047744981E-17));
#8650=CARTESIAN_POINT('',(-0.0866025403784438,-0.4,-0.15));
#8651=CARTESIAN_POINT('',(-0.173205080756888,-0.64,-2.77555756156289E-17));
#8652=CARTESIAN_POINT('',(-0.173205080756888,-0.4,-2.12115047744981E-17));
#8653=CARTESIAN_POINT('',(-0.0866025403784438,-0.64,-0.15));
#8654=CARTESIAN_POINT('Origin',(-0.0866025403784439,-0.4,0.15));
#8655=CARTESIAN_POINT('',(-0.0866025403784439,-0.4,0.15));
#8656=CARTESIAN_POINT('',(-0.173205080756888,-0.4,-2.12115047744981E-17));
#8657=CARTESIAN_POINT('',(-0.0866025403784439,-0.64,0.15));
#8658=CARTESIAN_POINT('',(-0.0866025403784439,-0.4,0.15));
#8659=CARTESIAN_POINT('',(-0.173205080756888,-0.64,-2.12115047744981E-17));
#8660=CARTESIAN_POINT('Origin',(0.0866025403784439,-0.4,0.15));
#8661=CARTESIAN_POINT('',(0.0866025403784439,-0.4,0.15));
#8662=CARTESIAN_POINT('',(-0.0866025403784439,-0.4,0.15));
#8663=CARTESIAN_POINT('',(0.0866025403784439,-0.64,0.15));
#8664=CARTESIAN_POINT('',(0.0866025403784439,-0.4,0.15));
#8665=CARTESIAN_POINT('',(-0.0866025403784439,-0.64,0.15));
#8666=CARTESIAN_POINT('Origin',(0.173205080756888,-0.4,0.));
#8667=CARTESIAN_POINT('',(0.0866025403784439,-0.4,0.15));
#8668=CARTESIAN_POINT('',(0.0866025403784439,-0.64,0.15));
#8669=CARTESIAN_POINT('Origin',(0.,-0.4,-2.77555756156289E-17));
#8670=CARTESIAN_POINT('Origin',(0.,-0.64,-2.77555756156289E-17));
#9063=UNCERTAINTY_MEASURE_WITH_UNIT(LENGTH_MEASURE(0.001),#9103,
'DISTANCE_ACCURACY_VALUE',
'Maximum model space distance between geometric entities at asserted c
onnectivities');
#9069=UNCERTAINTY_MEASURE_WITH_UNIT(LENGTH_MEASURE(0.001),#9103,
'DISTANCE_ACCURACY_VALUE',
'Maximum model space distance between geometric entities at asserted c
onnectivities');
#9096=(
GEOMETRIC_REPRESENTATION_CONTEXT(3)
GLOBAL_UNCERTAINTY_ASSIGNED_CONTEXT((#9063))
GLOBAL_UNIT_ASSIGNED_CONTEXT((#9103,#9105,#9106))
REPRESENTATION_CONTEXT('','3D')
);
#9102=(
GEOMETRIC_REPRESENTATION_CONTEXT(3)
GLOBAL_UNCERTAINTY_ASSIGNED_CONTEXT((#9069))
GLOBAL_UNIT_ASSIGNED_CONTEXT((#9103,#9105,#9106))
REPRESENTATION_CONTEXT('','3D')
);
#9103=(
LENGTH_UNIT()
NAMED_UNIT(*)
SI_UNIT(.CENTI.,.METRE.)
);
#9105=(
NAMED_UNIT(*)
PLANE_ANGLE_UNIT()
SI_UNIT($,.RADIAN.)
);
#9106=(
NAMED_UNIT(*)
SI_UNIT($,.STERADIAN.)
SOLID_ANGLE_UNIT()
);
#9133=SHAPE_DEFINITION_REPRESENTATION(#9208,#9253);
#9208=PRODUCT_DEFINITION_SHAPE('',$,#9286);
#9253=SHAPE_REPRESENTATION('',(#5773),#9096);
#9259=PRODUCT_DEFINITION_CONTEXT('part definition',#9357,'design');
#9286=PRODUCT_DEFINITION('Cap Screw - M4x16','Cap Screw - M4x16',#9318,
#9259);
#9318=PRODUCT_DEFINITION_FORMATION('',$,#9385);
#9357=APPLICATION_CONTEXT(
'Core Data for Automotive Mechanical Design Process');
#9358=PRODUCT_CONTEXT('part definition',#9357,'mechanical');
#9385=PRODUCT('Cap Screw - M4x16','Cap Screw - M4x16',
'Cap Screw - M4x16',(#9358));
#9461=COLOUR_RGB('Black',0.12,0.14,0.17);
#9462=FILL_AREA_STYLE_COLOUR('',#9461);
#9463=FILL_AREA_STYLE('',(#9462));
#9464=SURFACE_STYLE_FILL_AREA(#9463);
#9465=SURFACE_SIDE_STYLE('',(#9464));
#9466=SURFACE_STYLE_USAGE(.BOTH.,#9465);
#9467=PRESENTATION_STYLE_ASSIGNMENT((#9466));
ENDSEC;
END-ISO-10303-21;
